ISO-10303-21;
HEADER;
/* Generated by software containing ST-Developer
 * from STEP Tools, Inc. (www.steptools.com) 
 */

FILE_DESCRIPTION(
/* description */ ('Flange-mounted spindle'),
/* implementation_level */ '2;1');

FILE_NAME(
/* name */ 'M6x18 mounting screw.step',
/* time_stamp */ '2026-10-27T10:49:51-07:00',
/* author */ (''),
/* organization */ (''),
/* preprocessor_version */ 'ST-DEVELOPER v20.2',
/* originating_system */ 'Autodesk Translation Framework v15.17.0.0',
/* authorisation */ '');

FILE_SCHEMA (('AUTOMOTIVE_DESIGN { 1 0 10303 214 3 1 1 }'));
ENDSEC;

DATA;
#10=MECHANICAL_DESIGN_GEOMETRIC_PRESENTATION_REPRESENTATION('',(#346),#11764);
#263=CONICAL_SURFACE('',#6567,0.475,0.785398163397449);
#264=CONICAL_SURFACE('',#6571,0.485,0.785398163397448);
#265=CONICAL_SURFACE('',#6575,0.31,0.463647609000806);
#278=ORIENTED_CLOSED_SHELL('',*,#6138,.F.);
#281=BREP_WITH_VOIDS('Body1',#6139,(#278));
#292=SHAPE_REPRESENTATION_RELATIONSHIP('SRR','None',#11888,#319);
#319=ADVANCED_BREP_SHAPE_REPRESENTATION('',(#281),#11743);
#346=STYLED_ITEM('',(#12106),#281);
#417=FACE_BOUND('',#1110,.T.);
#540=PLANE('',#6555);
#541=PLANE('',#6556);
#542=PLANE('',#6557);
#543=PLANE('',#6558);
#544=PLANE('',#6559);
#545=PLANE('',#6560);
#546=PLANE('',#6561);
#547=PLANE('',#6562);
#548=PLANE('',#6563);
#549=PLANE('',#6565);
#550=PLANE('',#6573);
#725=FACE_OUTER_BOUND('',#1096,.T.);
#726=FACE_OUTER_BOUND('',#1097,.T.);
#727=FACE_OUTER_BOUND('',#1098,.T.);
#728=FACE_OUTER_BOUND('',#1099,.T.);
#729=FACE_OUTER_BOUND('',#1100,.T.);
#730=FACE_OUTER_BOUND('',#1101,.T.);
#731=FACE_OUTER_BOUND('',#1102,.T.);
#732=FACE_OUTER_BOUND('',#1103,.T.);
#733=FACE_OUTER_BOUND('',#1104,.T.);
#734=FACE_OUTER_BOUND('',#1105,.T.);
#735=FACE_OUTER_BOUND('',#1106,.T.);
#736=FACE_OUTER_BOUND('',#1107,.T.);
#737=FACE_OUTER_BOUND('',#1108,.T.);
#738=FACE_OUTER_BOUND('',#1109,.T.);
#739=FACE_OUTER_BOUND('',#1111,.T.);
#740=FACE_OUTER_BOUND('',#1112,.T.);
#1096=EDGE_LOOP('',(#4215,#4216,#4217,#4218));
#1097=EDGE_LOOP('',(#4219,#4220,#4221,#4222));
#1098=EDGE_LOOP('',(#4223,#4224,#4225,#4226));
#1099=EDGE_LOOP('',(#4227,#4228,#4229,#4230));
#1100=EDGE_LOOP('',(#4231,#4232,#4233,#4234));
#1101=EDGE_LOOP('',(#4235,#4236,#4237,#4238));
#1102=EDGE_LOOP('',(#4239,#4240,#4241,#4242,#4243,#4244));
#1103=EDGE_LOOP('',(#4245,#4246,#4247,#4248,#4249,#4250));
#1104=EDGE_LOOP('',(#4251));
#1105=EDGE_LOOP('',(#4252));
#1106=EDGE_LOOP('',(#4253,#4254,#4255,#4256));
#1107=EDGE_LOOP('',(#4257,#4258,#4259,#4260));
#1108=EDGE_LOOP('',(#4261,#4262,#4263,#4264));
#1109=EDGE_LOOP('',(#4265));
#1110=EDGE_LOOP('',(#4266));
#1111=EDGE_LOOP('',(#4267,#4268,#4269,#4270));
#1112=EDGE_LOOP('',(#4271,#4272,#4273,#4274));
#1550=LINE('',#9368,#1972);
#1551=LINE('',#9370,#1973);
#1552=LINE('',#9372,#1974);
#1553=LINE('',#9373,#1975);
#1554=LINE('',#9376,#1976);
#1555=LINE('',#9378,#1977);
#1556=LINE('',#9379,#1978);
#1557=LINE('',#9382,#1979);
#1558=LINE('',#9384,#1980);
#1559=LINE('',#9385,#1981);
#1560=LINE('',#9388,#1982);
#1561=LINE('',#9390,#1983);
#1562=LINE('',#9391,#1984);
#1563=LINE('',#9394,#1985);
#1564=LINE('',#9396,#1986);
#1565=LINE('',#9397,#1987);
#1566=LINE('',#9399,#1988);
#1567=LINE('',#9400,#1989);
#1568=LINE('',#9412,#1990);
#1569=LINE('',#9416,#1991);
#1570=LINE('',#9420,#1992);
#1571=LINE('',#9427,#1993);
#1572=LINE('',#9429,#1994);
#1972=VECTOR('',#7473,1.);
#1973=VECTOR('',#7474,1.);
#1974=VECTOR('',#7475,1.);
#1975=VECTOR('',#7476,1.);
#1976=VECTOR('',#7479,1.);
#1977=VECTOR('',#7480,1.);
#1978=VECTOR('',#7481,1.);
#1979=VECTOR('',#7484,1.);
#1980=VECTOR('',#7485,1.);
#1981=VECTOR('',#7486,1.);
#1982=VECTOR('',#7489,1.);
#1983=VECTOR('',#7490,1.);
#1984=VECTOR('',#7491,1.);
#1985=VECTOR('',#7494,1.);
#1986=VECTOR('',#7495,1.);
#1987=VECTOR('',#7496,1.);
#1988=VECTOR('',#7499,1.);
#1989=VECTOR('',#7500,1.);
#1990=VECTOR('',#7517,0.475);
#1991=VECTOR('',#7522,0.5);
#1992=VECTOR('',#7527,0.485);
#1993=VECTOR('',#7536,0.31);
#1994=VECTOR('',#7539,0.3);
#2357=CIRCLE('',#6564,0.2942);
#2358=CIRCLE('',#6566,0.45);
#2359=CIRCLE('',#6568,0.5);
#2360=CIRCLE('',#6570,0.5);
#2361=CIRCLE('',#6572,0.47);
#2362=CIRCLE('',#6574,0.32);
#2363=CIRCLE('',#6576,0.2942);
#2719=VERTEX_POINT('',#9366);
#2720=VERTEX_POINT('',#9367);
#2721=VERTEX_POINT('',#9369);
#2722=VERTEX_POINT('',#9371);
#2723=VERTEX_POINT('',#9375);
#2724=VERTEX_POINT('',#9377);
#2725=VERTEX_POINT('',#9381);
#2726=VERTEX_POINT('',#9383);
#2727=VERTEX_POINT('',#9387);
#2728=VERTEX_POINT('',#9389);
#2729=VERTEX_POINT('',#9393);
#2730=VERTEX_POINT('',#9395);
#2731=VERTEX_POINT('',#9404);
#2732=VERTEX_POINT('',#9407);
#2733=VERTEX_POINT('',#9410);
#2734=VERTEX_POINT('',#9414);
#2735=VERTEX_POINT('',#9418);
#2736=VERTEX_POINT('',#9422);
#2737=VERTEX_POINT('',#9425);
#3300=EDGE_CURVE('',#2719,#2720,#1550,.T.);
#3301=EDGE_CURVE('',#2720,#2721,#1551,.T.);
#3302=EDGE_CURVE('',#2721,#2722,#1552,.T.);
#3303=EDGE_CURVE('',#2719,#2722,#1553,.T.);
#3304=EDGE_CURVE('',#2720,#2723,#1554,.T.);
#3305=EDGE_CURVE('',#2723,#2724,#1555,.T.);
#3306=EDGE_CURVE('',#2724,#2721,#1556,.T.);
#3307=EDGE_CURVE('',#2723,#2725,#1557,.T.);
#3308=EDGE_CURVE('',#2725,#2726,#1558,.T.);
#3309=EDGE_CURVE('',#2726,#2724,#1559,.T.);
#3310=EDGE_CURVE('',#2725,#2727,#1560,.T.);
#3311=EDGE_CURVE('',#2727,#2728,#1561,.T.);
#3312=EDGE_CURVE('',#2728,#2726,#1562,.T.);
#3313=EDGE_CURVE('',#2727,#2729,#1563,.T.);
#3314=EDGE_CURVE('',#2729,#2730,#1564,.T.);
#3315=EDGE_CURVE('',#2730,#2728,#1565,.T.);
#3316=EDGE_CURVE('',#2729,#2719,#1566,.T.);
#3317=EDGE_CURVE('',#2722,#2730,#1567,.T.);
#3318=EDGE_CURVE('',#2731,#2731,#2357,.T.);
#3319=EDGE_CURVE('',#2732,#2732,#2358,.T.);
#3320=EDGE_CURVE('',#2733,#2733,#2359,.T.);
#3321=EDGE_CURVE('',#2733,#2732,#1568,.T.);
#3322=EDGE_CURVE('',#2734,#2734,#2360,.T.);
#3323=EDGE_CURVE('',#2734,#2733,#1569,.T.);
#3324=EDGE_CURVE('',#2735,#2735,#2361,.T.);
#3325=EDGE_CURVE('',#2735,#2734,#1570,.T.);
#3326=EDGE_CURVE('',#2736,#2736,#2362,.T.);
#3327=EDGE_CURVE('',#2737,#2737,#2363,.F.);
#3328=EDGE_CURVE('',#2737,#2736,#1571,.T.);
#3329=EDGE_CURVE('',#2731,#2737,#1572,.T.);
#4215=ORIENTED_EDGE('',*,*,#3300,.T.);
#4216=ORIENTED_EDGE('',*,*,#3301,.T.);
#4217=ORIENTED_EDGE('',*,*,#3302,.T.);
#4218=ORIENTED_EDGE('',*,*,#3303,.F.);
#4219=ORIENTED_EDGE('',*,*,#3304,.T.);
#4220=ORIENTED_EDGE('',*,*,#3305,.T.);
#4221=ORIENTED_EDGE('',*,*,#3306,.T.);
#4222=ORIENTED_EDGE('',*,*,#3301,.F.);
#4223=ORIENTED_EDGE('',*,*,#3307,.T.);
#4224=ORIENTED_EDGE('',*,*,#3308,.T.);
#4225=ORIENTED_EDGE('',*,*,#3309,.T.);
#4226=ORIENTED_EDGE('',*,*,#3305,.F.);
#4227=ORIENTED_EDGE('',*,*,#3310,.T.);
#4228=ORIENTED_EDGE('',*,*,#3311,.T.);
#4229=ORIENTED_EDGE('',*,*,#3312,.T.);
#4230=ORIENTED_EDGE('',*,*,#3308,.F.);
#4231=ORIENTED_EDGE('',*,*,#3313,.T.);
#4232=ORIENTED_EDGE('',*,*,#3314,.T.);
#4233=ORIENTED_EDGE('',*,*,#3315,.T.);
#4234=ORIENTED_EDGE('',*,*,#3311,.F.);
#4235=ORIENTED_EDGE('',*,*,#3316,.T.);
#4236=ORIENTED_EDGE('',*,*,#3303,.T.);
#4237=ORIENTED_EDGE('',*,*,#3317,.T.);
#4238=ORIENTED_EDGE('',*,*,#3314,.F.);
#4239=ORIENTED_EDGE('',*,*,#3316,.F.);
#4240=ORIENTED_EDGE('',*,*,#3313,.F.);
#4241=ORIENTED_EDGE('',*,*,#3310,.F.);
#4242=ORIENTED_EDGE('',*,*,#3307,.F.);
#4243=ORIENTED_EDGE('',*,*,#3304,.F.);
#4244=ORIENTED_EDGE('',*,*,#3300,.F.);
#4245=ORIENTED_EDGE('',*,*,#3317,.F.);
#4246=ORIENTED_EDGE('',*,*,#3302,.F.);
#4247=ORIENTED_EDGE('',*,*,#3306,.F.);
#4248=ORIENTED_EDGE('',*,*,#3309,.F.);
#4249=ORIENTED_EDGE('',*,*,#3312,.F.);
#4250=ORIENTED_EDGE('',*,*,#3315,.F.);
#4251=ORIENTED_EDGE('',*,*,#3318,.F.);
#4252=ORIENTED_EDGE('',*,*,#3319,.F.);
#4253=ORIENTED_EDGE('',*,*,#3320,.F.);
#4254=ORIENTED_EDGE('',*,*,#3321,.T.);
#4255=ORIENTED_EDGE('',*,*,#3319,.T.);
#4256=ORIENTED_EDGE('',*,*,#3321,.F.);
#4257=ORIENTED_EDGE('',*,*,#3322,.F.);
#4258=ORIENTED_EDGE('',*,*,#3323,.T.);
#4259=ORIENTED_EDGE('',*,*,#3320,.T.);
#4260=ORIENTED_EDGE('',*,*,#3323,.F.);
#4261=ORIENTED_EDGE('',*,*,#3324,.F.);
#4262=ORIENTED_EDGE('',*,*,#3325,.T.);
#4263=ORIENTED_EDGE('',*,*,#3322,.T.);
#4264=ORIENTED_EDGE('',*,*,#3325,.F.);
#4265=ORIENTED_EDGE('',*,*,#3324,.T.);
#4266=ORIENTED_EDGE('',*,*,#3326,.F.);
#4267=ORIENTED_EDGE('',*,*,#3327,.F.);
#4268=ORIENTED_EDGE('',*,*,#3328,.T.);
#4269=ORIENTED_EDGE('',*,*,#3326,.T.);
#4270=ORIENTED_EDGE('',*,*,#3328,.F.);
#4271=ORIENTED_EDGE('',*,*,#3318,.T.);
#4272=ORIENTED_EDGE('',*,*,#3329,.T.);
#4273=ORIENTED_EDGE('',*,*,#3327,.T.);
#4274=ORIENTED_EDGE('',*,*,#3329,.F.);
#5642=CYLINDRICAL_SURFACE('',#6569,0.5);
#5643=CYLINDRICAL_SURFACE('',#6577,0.2942);
#5836=ADVANCED_FACE('',(#725),#540,.F.);
#5837=ADVANCED_FACE('',(#726),#541,.F.);
#5838=ADVANCED_FACE('',(#727),#542,.F.);
#5839=ADVANCED_FACE('',(#728),#543,.F.);
#5840=ADVANCED_FACE('',(#729),#544,.F.);
#5841=ADVANCED_FACE('',(#730),#545,.F.);
#5842=ADVANCED_FACE('',(#731),#546,.F.);
#5843=ADVANCED_FACE('',(#732),#547,.F.);
#5844=ADVANCED_FACE('',(#733),#548,.F.);
#5845=ADVANCED_FACE('',(#734),#549,.T.);
#5846=ADVANCED_FACE('',(#735),#263,.T.);
#5847=ADVANCED_FACE('',(#736),#5642,.T.);
#5848=ADVANCED_FACE('',(#737),#264,.T.);
#5849=ADVANCED_FACE('',(#738,#417),#550,.T.);
#5850=ADVANCED_FACE('',(#739),#265,.T.);
#5851=ADVANCED_FACE('',(#740),#5643,.T.);
#6138=CLOSED_SHELL('',(#5836,#5837,#5838,#5839,#5840,#5841,#5842,#5843));
#6139=CLOSED_SHELL('',(#5844,#5845,#5846,#5847,#5848,#5849,#5850,#5851));
#6554=AXIS2_PLACEMENT_3D('',#9364,#7469,#7470);
#6555=AXIS2_PLACEMENT_3D('',#9365,#7471,#7472);
#6556=AXIS2_PLACEMENT_3D('',#9374,#7477,#7478);
#6557=AXIS2_PLACEMENT_3D('',#9380,#7482,#7483);
#6558=AXIS2_PLACEMENT_3D('',#9386,#7487,#7488);
#6559=AXIS2_PLACEMENT_3D('',#9392,#7492,#7493);
#6560=AXIS2_PLACEMENT_3D('',#9398,#7497,#7498);
#6561=AXIS2_PLACEMENT_3D('',#9401,#7501,#7502);
#6562=AXIS2_PLACEMENT_3D('',#9402,#7503,#7504);
#6563=AXIS2_PLACEMENT_3D('',#9403,#7505,#7506);
#6564=AXIS2_PLACEMENT_3D('',#9405,#7507,#7508);
#6565=AXIS2_PLACEMENT_3D('',#9406,#7509,#7510);
#6566=AXIS2_PLACEMENT_3D('',#9408,#7511,#7512);
#6567=AXIS2_PLACEMENT_3D('',#9409,#7513,#7514);
#6568=AXIS2_PLACEMENT_3D('',#9411,#7515,#7516);
#6569=AXIS2_PLACEMENT_3D('',#9413,#7518,#7519);
#6570=AXIS2_PLACEMENT_3D('',#9415,#7520,#7521);
#6571=AXIS2_PLACEMENT_3D('',#9417,#7523,#7524);
#6572=AXIS2_PLACEMENT_3D('',#9419,#7525,#7526);
#6573=AXIS2_PLACEMENT_3D('',#9421,#7528,#7529);
#6574=AXIS2_PLACEMENT_3D('',#9423,#7530,#7531);
#6575=AXIS2_PLACEMENT_3D('',#9424,#7532,#7533);
#6576=AXIS2_PLACEMENT_3D('',#9426,#7534,#7535);
#6577=AXIS2_PLACEMENT_3D('',#9428,#7537,#7538);
#7469=DIRECTION('axis',(0.,0.,1.));
#7470=DIRECTION('refdir',(1.,0.,0.));
#7471=DIRECTION('center_axis',(0.866025403784439,0.,-0.5));
#7472=DIRECTION('ref_axis',(0.5,0.,0.866025403784439));
#7473=DIRECTION('',(-0.5,0.,-0.866025403784439));
#7474=DIRECTION('',(0.,-1.,0.));
#7475=DIRECTION('',(0.5,0.,0.866025403784439));
#7476=DIRECTION('',(0.,-1.,0.));
#7477=DIRECTION('center_axis',(1.92296268638356E-16,0.,-1.));
#7478=DIRECTION('ref_axis',(1.,0.,1.92296268638356E-16));
#7479=DIRECTION('',(-1.,0.,-1.92296268638356E-16));
#7480=DIRECTION('',(0.,-1.,0.));
#7481=DIRECTION('',(1.,0.,1.92296268638356E-16));
#7482=DIRECTION('center_axis',(-0.866025403784439,0.,-0.5));
#7483=DIRECTION('ref_axis',(0.5,0.,-0.866025403784439));
#7484=DIRECTION('',(-0.5,0.,0.866025403784438));
#7485=DIRECTION('',(0.,-1.,0.));
#7486=DIRECTION('',(0.5,0.,-0.866025403784438));
#7487=DIRECTION('center_axis',(-0.866025403784439,0.,0.5));
#7488=DIRECTION('ref_axis',(-0.5,0.,-0.866025403784439));
#7489=DIRECTION('',(0.5,0.,0.866025403784439));
#7490=DIRECTION('',(0.,-1.,0.));
#7491=DIRECTION('',(-0.5,0.,-0.866025403784439));
#7492=DIRECTION('center_axis',(-1.92296268638356E-16,0.,1.));
#7493=DIRECTION('ref_axis',(-1.,0.,-1.92296268638356E-16));
#7494=DIRECTION('',(1.,0.,1.92296268638356E-16));
#7495=DIRECTION('',(0.,-1.,0.));
#7496=DIRECTION('',(-1.,0.,-1.92296268638356E-16));
#7497=DIRECTION('center_axis',(0.866025403784439,0.,0.5));
#7498=DIRECTION('ref_axis',(-0.5,0.,0.866025403784439));
#7499=DIRECTION('',(0.5,0.,-0.866025403784439));
#7500=DIRECTION('',(-0.5,0.,0.866025403784439));
#7501=DIRECTION('center_axis',(0.,1.,0.));
#7502=DIRECTION('ref_axis',(1.,0.,0.));
#7503=DIRECTION('center_axis',(0.,-1.,0.));
#7504=DIRECTION('ref_axis',(0.,0.,-1.));
#7505=DIRECTION('center_axis',(0.,1.,0.));
#7506=DIRECTION('ref_axis',(1.,0.,0.));
#7507=DIRECTION('center_axis',(0.,1.,0.));
#7508=DIRECTION('ref_axis',(1.,0.,0.));
#7509=DIRECTION('center_axis',(0.,1.,0.));
#7510=DIRECTION('ref_axis',(0.,0.,1.));
#7511=DIRECTION('center_axis',(0.,-1.,0.));
#7512=DIRECTION('ref_axis',(1.,0.,0.));
#7513=DIRECTION('center_axis',(0.,-1.,0.));
#7514=DIRECTION('ref_axis',(1.,0.,0.));
#7515=DIRECTION('center_axis',(0.,-1.,0.));
#7516=DIRECTION('ref_axis',(1.,0.,0.));
#7517=DIRECTION('',(0.707106781186548,0.707106781186547,8.65956056235494E-17));
#7518=DIRECTION('center_axis',(0.,-1.,0.));
#7519=DIRECTION('ref_axis',(1.,0.,0.));
#7520=DIRECTION('center_axis',(0.,-1.,0.));
#7521=DIRECTION('ref_axis',(1.,0.,0.));
#7522=DIRECTION('',(0.,1.,0.));
#7523=DIRECTION('center_axis',(0.,1.,0.));
#7524=DIRECTION('ref_axis',(1.,0.,0.));
#7525=DIRECTION('center_axis',(0.,-1.,0.));
#7526=DIRECTION('ref_axis',(1.,0.,0.));
#7527=DIRECTION('',(-0.707106781186547,0.707106781186548,-8.65956056235493E-17));
#7528=DIRECTION('center_axis',(0.,-1.,0.));
#7529=DIRECTION('ref_axis',(0.,0.,-1.));
#7530=DIRECTION('center_axis',(0.,-1.,0.));
#7531=DIRECTION('ref_axis',(1.,0.,0.));
#7532=DIRECTION('center_axis',(0.,1.,0.));
#7533=DIRECTION('ref_axis',(1.,0.,0.));
#7534=DIRECTION('center_axis',(0.,1.,0.));
#7535=DIRECTION('ref_axis',(1.,0.,0.));
#7536=DIRECTION('',(-0.447213595499958,0.894427190999916,-5.47678698264203E-17));
#7537=DIRECTION('center_axis',(0.,-1.,0.));
#7538=DIRECTION('ref_axis',(1.,0.,0.));
#7539=DIRECTION('',(0.,1.,0.));
#9364=CARTESIAN_POINT('',(0.,0.,0.));
#9365=CARTESIAN_POINT('Origin',(0.144337567297406,-0.6,-0.25));
#9366=CARTESIAN_POINT('',(0.288675134594813,-0.6,0.));
#9367=CARTESIAN_POINT('',(0.144337567297406,-0.6,-0.25));
#9368=CARTESIAN_POINT('',(0.288675134594813,-0.6,0.));
#9369=CARTESIAN_POINT('',(0.144337567297406,-0.96,-0.25));
#9370=CARTESIAN_POINT('',(0.144337567297406,-0.6,-0.25));
#9371=CARTESIAN_POINT('',(0.288675134594813,-0.96,0.));
#9372=CARTESIAN_POINT('',(0.288675134594813,-0.96,0.));
#9373=CARTESIAN_POINT('',(0.288675134594813,-0.6,0.));
#9374=CARTESIAN_POINT('Origin',(-0.144337567297406,-0.6,-0.25));
#9375=CARTESIAN_POINT('',(-0.144337567297406,-0.6,-0.25));
#9376=CARTESIAN_POINT('',(0.144337567297406,-0.6,-0.25));
#9377=CARTESIAN_POINT('',(-0.144337567297406,-0.96,-0.25));
#9378=CARTESIAN_POINT('',(-0.144337567297406,-0.6,-0.25));
#9379=CARTESIAN_POINT('',(0.144337567297406,-0.96,-0.25));
#9380=CARTESIAN_POINT('Origin',(-0.288675134594813,-0.6,-8.32667268468867E-17));
#9381=CARTESIAN_POINT('',(-0.288675134594813,-0.6,-3.53525079574969E-17));
#9382=CARTESIAN_POINT('',(-0.144337567297406,-0.6,-0.25));
#9383=CARTESIAN_POINT('',(-0.288675134594813,-0.96,-5.55111512312578E-17));
#9384=CARTESIAN_POINT('',(-0.288675134594813,-0.6,-3.53525079574969E-17));
#9385=CARTESIAN_POINT('',(-0.144337567297406,-0.96,-0.25));
#9386=CARTESIAN_POINT('Origin',(-0.144337567297407,-0.6,0.25));
#9387=CARTESIAN_POINT('',(-0.144337567297407,-0.6,0.25));
#9388=CARTESIAN_POINT('',(-0.288675134594813,-0.6,-3.53525079574969E-17));
#9389=CARTESIAN_POINT('',(-0.144337567297407,-0.96,0.25));
#9390=CARTESIAN_POINT('',(-0.144337567297407,-0.6,0.25));
#9391=CARTESIAN_POINT('',(-0.288675134594813,-0.96,-3.53525079574969E-17));
#9392=CARTESIAN_POINT('Origin',(0.144337567297406,-0.6,0.25));
#9393=CARTESIAN_POINT('',(0.144337567297406,-0.6,0.25));
#9394=CARTESIAN_POINT('',(-0.144337567297407,-0.6,0.25));
#9395=CARTESIAN_POINT('',(0.144337567297406,-0.96,0.25));
#9396=CARTESIAN_POINT('',(0.144337567297406,-0.6,0.25));
#9397=CARTESIAN_POINT('',(-0.144337567297407,-0.96,0.25));
#9398=CARTESIAN_POINT('Origin',(0.288675134594813,-0.6,0.));
#9399=CARTESIAN_POINT('',(0.144337567297406,-0.6,0.25));
#9400=CARTESIAN_POINT('',(0.144337567297406,-0.96,0.25));
#9401=CARTESIAN_POINT('Origin',(0.,-0.6,0.));
#9402=CARTESIAN_POINT('Origin',(0.,-0.96,0.));
#9403=CARTESIAN_POINT('Origin',(0.,-1.8,0.));
#9404=CARTESIAN_POINT('',(-0.2942,-1.8,3.60291088309151E-17));
#9405=CARTESIAN_POINT('Origin',(0.,-1.8,0.));
#9406=CARTESIAN_POINT('Origin',(0.45,0.6,0.));
#9407=CARTESIAN_POINT('',(-0.45,0.6,-5.51091059616309E-17));
#9408=CARTESIAN_POINT('Origin',(0.,0.6,0.));
#9409=CARTESIAN_POINT('Origin',(0.,0.575,0.));
#9410=CARTESIAN_POINT('',(-0.5,0.55,-6.12323399573677E-17));
#9411=CARTESIAN_POINT('Origin',(0.,0.55,0.));
#9412=CARTESIAN_POINT('',(-0.475,0.575,-5.81707229594993E-17));
#9413=CARTESIAN_POINT('Origin',(0.,0.29,0.));
#9414=CARTESIAN_POINT('',(-0.5,0.0299999999999998,-6.12323399573677E-17));
#9415=CARTESIAN_POINT('Origin',(0.,0.0299999999999998,0.));
#9416=CARTESIAN_POINT('',(-0.5,0.29,-6.12323399573677E-17));
#9417=CARTESIAN_POINT('Origin',(0.,0.0150000000000001,0.));
#9418=CARTESIAN_POINT('',(-0.47,7.11236625150491E-17,-5.75583995599256E-17));
#9419=CARTESIAN_POINT('Origin',(0.,0.,0.));
#9420=CARTESIAN_POINT('',(-0.485,0.0150000000000001,-5.93953697586466E-17));
#9421=CARTESIAN_POINT('Origin',(0.32,0.,0.));
#9422=CARTESIAN_POINT('',(-0.32,-6.93889390390723E-18,-3.91886975727153E-17));
#9423=CARTESIAN_POINT('Origin',(0.,0.,0.));
#9424=CARTESIAN_POINT('Origin',(0.,-0.02,0.));
#9425=CARTESIAN_POINT('',(-0.2942,-0.0515999999999999,3.60291088309151E-17));
#9426=CARTESIAN_POINT('Origin',(0.,-0.0515999999999999,0.));
#9427=CARTESIAN_POINT('',(-0.31,-0.02,-3.7964050773568E-17));
#9428=CARTESIAN_POINT('Origin',(0.,-1.24,0.));
#9429=CARTESIAN_POINT('',(-0.2942,-1.24,-3.60291088309151E-17));
#11711=UNCERTAINTY_MEASURE_WITH_UNIT(LENGTH_MEASURE(0.001),#11765,
'DISTANCE_ACCURACY_VALUE',
'Maximum model space distance between geometric entities at asserted c
onnectivities');
#11732=UNCERTAINTY_MEASURE_WITH_UNIT(LENGTH_MEASURE(0.001),#11765,
'DISTANCE_ACCURACY_VALUE',
'Maximum model space distance between geometric entities at asserted c
onnectivities');
#11743=(
GEOMETRIC_REPRESENTATION_CONTEXT(3)
GLOBAL_UNCERTAINTY_ASSIGNED_CONTEXT((#11711))
GLOBAL_UNIT_ASSIGNED_CONTEXT((#11765,#11767,#11768))
REPRESENTATION_CONTEXT('','3D')
);
#11764=(
GEOMETRIC_REPRESENTATION_CONTEXT(3)
GLOBAL_UNCERTAINTY_ASSIGNED_CONTEXT((#11732))
GLOBAL_UNIT_ASSIGNED_CONTEXT((#11765,#11767,#11768))
REPRESENTATION_CONTEXT('','3D')
);
#11765=(
LENGTH_UNIT()
NAMED_UNIT(*)
SI_UNIT(.CENTI.,.METRE.)
);
#11767=(
NAMED_UNIT(*)
PLANE_ANGLE_UNIT()
SI_UNIT($,.RADIAN.)
);
#11768=(
NAMED_UNIT(*)
SI_UNIT($,.STERADIAN.)
SOLID_ANGLE_UNIT()
);
#11779=SHAPE_DEFINITION_REPRESENTATION(#11810,#11888);
#11810=PRODUCT_DEFINITION_SHAPE('',$,#11920);
#11888=SHAPE_REPRESENTATION('',(#6554),#11743);
#11909=PRODUCT_DEFINITION_CONTEXT('part definition',#12004,'design');
#11920=PRODUCT_DEFINITION('M6x18 mounting screw','M6x18 mounting screw',
#11951,#11909);
#11951=PRODUCT_DEFINITION_FORMATION('',$,#12016);
#12004=APPLICATION_CONTEXT(
'Core Data for Automotive Mechanical Design Process');
#12005=PRODUCT_CONTEXT('part definition',#12004,'mechanical');
#12016=PRODUCT('M6x18 mounting screw','M6x18 mounting screw',
'M6x18 mounting screw',(#12005));
#12100=COLOUR_RGB('Black',0.12,0.14,0.17);
#12101=FILL_AREA_STYLE_COLOUR('',#12100);
#12102=FILL_AREA_STYLE('',(#12101));
#12103=SURFACE_STYLE_FILL_AREA(#12102);
#12104=SURFACE_SIDE_STYLE('',(#12103));
#12105=SURFACE_STYLE_USAGE(.BOTH.,#12104);
#12106=PRESENTATION_STYLE_ASSIGNMENT((#12105));
ENDSEC;
END-ISO-10303-21;
